ISO-10303-21;
HEADER;
FILE_DESCRIPTION (('STEP AP214'),
    '1' );
FILE_NAME ('o-rings series a_iso_O-ring 19x1.8-A-ISO 3601-1.step',
    '2026-09-24T10:28:59',
    ( '' ),
    ( '' ),
    'SwSTEP 2.0',
    'SolidWorks 2026',
    '' );
FILE_SCHEMA (( 'AUTOMOTIVE_DESIGN' ));
ENDSEC;

DATA;
#133=VERTEX_POINT ( 'NONE', #2641 ) ;
#136=CARTESIAN_POINT ( 'NONE',  ( 0.000000000000000000, 0.000000000000000000, 0.000000000000000000 ) ) ;
#148=EDGE_LOOP ( 'NONE', ( #1703, #3321, #10614, #8753 ) ) ;
#165=( LENGTH_UNIT ( ) NAMED_UNIT ( * ) SI_UNIT ( .MILLI., .METRE. ) );
#211=ORIENTED_EDGE ( 'NONE', *, *, #16657, .F. ) ;
#433=ORIENTED_EDGE ( 'NONE', *, *, #8405, .T. ) ;
#441=ORIENTED_EDGE ( 'NONE', *, *, #16657, .T. ) ;
#500=CARTESIAN_POINT ( 'NONE',  ( 0.000000000000000000, 0.000000000000000000, 0.000000000000000000 ) ) ;
#526=( NAMED_UNIT ( * ) SI_UNIT ( $, .STERADIAN. ) SOLID_ANGLE_UNIT ( ) );
#686=EDGE_CURVE ( 'NONE', #133, #7467, #16259, .T. ) ;
#864=AXIS2_PLACEMENT_3D ( 'NONE', #2854, #2504, #5472 ) ;
#898=AXIS2_PLACEMENT_3D ( 'NONE', #1568, #4458, #11058 ) ;
#962=STYLED_ITEM ( 'NONE', ( #1134 ), #17490 ) ;
#986=ORIENTED_EDGE ( 'NONE', *, *, #7868, .T. ) ;
#1043=DIRECTION ( 'NONE',  ( 0.000000000000000000, 0.000000000000000000, -1.000000000000000000 ) ) ;
#1054=( NAMED_UNIT ( * ) SI_UNIT ( $, .STERADIAN. ) SOLID_ANGLE_UNIT ( ) );
#1134=PRESENTATION_STYLE_ASSIGNMENT (( #9546 ) ) ;
#1568=CARTESIAN_POINT ( 'NONE',  ( 0.000000000000000000, 0.000000000000000000, 1.102182119232618281E-16 ) ) ;
#1703=ORIENTED_EDGE ( 'NONE', *, *, #9712, .F. ) ;
#2036=AXIS2_PLACEMENT_3D ( 'NONE', #500, #8566, #7042 ) ;
#2081=SHAPE_REPRESENTATION ( 'o-rings series a_iso_O-ring 19x1.8-A-ISO 3601-1', ( #3575 ), #11602 ) ;
#2340=SURFACE_STYLE_FILL_AREA ( #17513 ) ;
#2411=CARTESIAN_POINT ( 'NONE',  ( -11.29999999999999893, 0.000000000000000000, 0.000000000000000000 ) ) ;
#2480=DIRECTION ( 'NONE',  ( -1.000000000000000000, 0.000000000000000000, 0.000000000000000000 ) ) ;
#2501=DIRECTION ( 'NONE',  ( -1.000000000000000000, 0.000000000000000000, 0.000000000000000000 ) ) ;
#2504=DIRECTION ( 'NONE',  ( -0.000000000000000000, -0.000000000000000000, -1.000000000000000000 ) ) ;
#2590=DIRECTION ( 'NONE',  ( -0.000000000000000000, -0.000000000000000000, -1.000000000000000000 ) ) ;
#2641=CARTESIAN_POINT ( 'NONE',  ( 9.500000000000000000, 1.163414459189985485E-15, 0.000000000000000000 ) ) ;
#2749=ORIENTED_EDGE ( 'NONE', *, *, #16433, .F. ) ;
#2854=CARTESIAN_POINT ( 'NONE',  ( 0.000000000000000000, 0.000000000000000000, 0.000000000000000000 ) ) ;
#2888=EDGE_LOOP ( 'NONE', ( #12997, #10963, #441, #14172 ) ) ;
#2980=( GEOMETRIC_REPRESENTATION_CONTEXT ( 3 ) GLOBAL_UNCERTAINTY_ASSIGNED_CONTEXT ( ( #14057 ) ) GLOBAL_UNIT_ASSIGNED_CONTEXT ( ( #7945, #5035, #1054 ) ) REPRESENTATION_CONTEXT ( 'NONE', 'WORKASPACE' ) );
#3122=DIRECTION ( 'NONE',  ( -1.224646799147353207E-16, 1.000000000000000000, 0.000000000000000000 ) ) ;
#3321=ORIENTED_EDGE ( 'NONE', *, *, #7868, .F. ) ;
#3575=AXIS2_PLACEMENT_3D ( 'NONE', #5095, #17575, #9272 ) ;
#3604=DIRECTION ( 'NONE',  ( 0.000000000000000000, -1.000000000000000000, 0.000000000000000000 ) ) ;
#3622=ORIENTED_EDGE ( 'NONE', *, *, #9712, .T. ) ;
#3803=COLOUR_RGB ( '', 0.66274510, 0.83137255, 0.94901961) ;
#3875=EDGE_CURVE ( 'NONE', #7467, #14045, #14107, .T. ) ;
#3891=DIRECTION ( 'NONE',  ( -1.224646799147353207E-16, 1.000000000000000000, 0.000000000000000000 ) ) ;
#4003=FACE_OUTER_BOUND ( 'NONE', #13112, .T. ) ;
#4102=AXIS2_PLACEMENT_3D ( 'NONE', #13720, #10704, #5276 ) ;
#4134=UNCERTAINTY_MEASURE_WITH_UNIT (LENGTH_MEASURE( 1.000000000000000082E-05 ), #12860, 'distance_accuracy_value', 'NONE');
#4423=COLOUR_RGB ( '', 0.66274510, 0.83137255, 0.94901961) ;
#4458=DIRECTION ( 'NONE',  ( -0.000000000000000000, -0.000000000000000000, -1.000000000000000000 ) ) ;
#5035=( NAMED_UNIT ( * ) PLANE_ANGLE_UNIT ( ) SI_UNIT ( $, .RADIAN. ) );
#5095=CARTESIAN_POINT ( 'NONE',  ( 0.000000000000000000, 0.000000000000000000, 0.000000000000000000 ) ) ;
#5202=FILL_AREA_STYLE_COLOUR ( '', #4423 ) ;
#5276=DIRECTION ( 'NONE',  ( -1.000000000000000000, 0.000000000000000000, 0.000000000000000000 ) ) ;
#5355=FACE_OUTER_BOUND ( 'NONE', #2888, .T. ) ;
#5384=FACE_OUTER_BOUND ( 'NONE', #148, .T. ) ;
#5398=TOROIDAL_SURFACE ( 'NONE', #864, 10.40000000000000036, 0.9000000000000003553 ) ;
#5472=DIRECTION ( 'NONE',  ( -1.000000000000000000, 0.000000000000000000, 0.000000000000000000 ) ) ;
#6313=CARTESIAN_POINT ( 'NONE',  ( -9.500000000000000000, 0.000000000000000000, 1.102182119232619020E-16 ) ) ;
#6449=DIRECTION ( 'NONE',  ( -1.000000000000000000, 0.000000000000000000, 0.000000000000000000 ) ) ;
#6453=AXIS2_PLACEMENT_3D ( 'NONE', #136, #2590, #2501 ) ;
#6498=SURFACE_SIDE_STYLE ('',( #2340 ) ) ;
#7042=DIRECTION ( 'NONE',  ( -1.000000000000000000, 0.000000000000000000, 0.000000000000000000 ) ) ;
#7156=( NAMED_UNIT ( * ) PLANE_ANGLE_UNIT ( ) SI_UNIT ( $, .RADIAN. ) );
#7197=ORIENTED_EDGE ( 'NONE', *, *, #10518, .T. ) ;
#7214=DIRECTION ( 'NONE',  ( -1.000000000000000000, -1.224646799147353454E-16, 0.000000000000000000 ) ) ;
#7309=CIRCLE ( 'NONE', #4102, 11.29999999999999893 ) ;
#7467=VERTEX_POINT ( 'NONE', #6313 ) ;
#7841=AXIS2_PLACEMENT_3D ( 'NONE', #8188, #12436, #2480 ) ;
#7852=STYLED_ITEM ( 'NONE', ( #10026 ), #14616 ) ;
#7868=EDGE_CURVE ( 'NONE', #133, #11061, #15635, .T. ) ;
#7887=DIRECTION ( 'NONE',  ( -1.000000000000000000, -1.224646799147353454E-16, 0.000000000000000000 ) ) ;
#7945=( LENGTH_UNIT ( ) NAMED_UNIT ( * ) SI_UNIT ( .MILLI., .METRE. ) );
#8082=DIRECTION ( 'NONE',  ( -0.000000000000000000, -0.000000000000000000, -1.000000000000000000 ) ) ;
#8105=CIRCLE ( 'NONE', #2036, 11.29999999999999893 ) ;
#8188=CARTESIAN_POINT ( 'NONE',  ( 0.000000000000000000, 0.000000000000000000, 0.000000000000000000 ) ) ;
#8405=EDGE_CURVE ( 'NONE', #14045, #7467, #17193, .T. ) ;
#8418=MECHANICAL_DESIGN_GEOMETRIC_PRESENTATION_REPRESENTATION('',(#7852),#14803);
#8442=TOROIDAL_SURFACE ( 'NONE', #9030, 10.40000000000000036, 0.9000000000000003553 ) ;
#8497=CIRCLE ( 'NONE', #10785, 0.8999999999999998002 ) ;
#8566=DIRECTION ( 'NONE',  ( -0.000000000000000000, -0.000000000000000000, -1.000000000000000000 ) ) ;
#8589=SURFACE_STYLE_FILL_AREA ( #14401 ) ;
#8753=ORIENTED_EDGE ( 'NONE', *, *, #3875, .T. ) ;
#8992=TOROIDAL_SURFACE ( 'NONE', #7841, 10.40000000000000036, 0.9000000000000003553 ) ;
#9030=AXIS2_PLACEMENT_3D ( 'NONE', #13971, #8082, #13617 ) ;
#9244=CARTESIAN_POINT ( 'NONE',  ( 0.000000000000000000, 0.000000000000000000, 1.102182119232618281E-16 ) ) ;
#9272=DIRECTION ( 'NONE',  ( 1.000000000000000000, 0.000000000000000000, 0.000000000000000000 ) ) ;
#9436=ADVANCED_FACE ( 'NONE', ( #5384 ), #5398, .T. ) ;
#9529=PRODUCT_DEFINITION_SHAPE ( 'NONE', 'NONE',  #12337 ) ;
#9546=SURFACE_STYLE_USAGE ( .BOTH. , #6498 ) ;
#9712=EDGE_CURVE ( 'NONE', #11061, #14045, #8105, .T. ) ;
#9937=FILL_AREA_STYLE_COLOUR ( '', #3803 ) ;
#10026=PRESENTATION_STYLE_ASSIGNMENT (( #14039 ) ) ;
#10191=SHAPE_DEFINITION_REPRESENTATION ( #9529, #2081 ) ;
#10518=EDGE_CURVE ( 'NONE', #7467, #133, #15377, .T. ) ;
#10614=ORIENTED_EDGE ( 'NONE', *, *, #686, .T. ) ;
#10704=DIRECTION ( 'NONE',  ( -0.000000000000000000, -0.000000000000000000, -1.000000000000000000 ) ) ;
#10785=AXIS2_PLACEMENT_3D ( 'NONE', #17800, #3891, #7887 ) ;
#10963=ORIENTED_EDGE ( 'NONE', *, *, #16433, .T. ) ;
#11058=DIRECTION ( 'NONE',  ( -1.000000000000000000, 0.000000000000000000, 0.000000000000000000 ) ) ;
#11061=VERTEX_POINT ( 'NONE', #14719 ) ;
#11133=ADVANCED_FACE ( 'NONE', ( #4003 ), #8442, .T. ) ;
#11179=PRODUCT_DEFINITION_FORMATION_WITH_SPECIFIED_SOURCE ( 'ANY', '', #13304, .NOT_KNOWN. ) ;
#11345=MECHANICAL_DESIGN_GEOMETRIC_PRESENTATION_REPRESENTATION('',(#962),#2980);
#11602=( GEOMETRIC_REPRESENTATION_CONTEXT ( 3 ) GLOBAL_UNCERTAINTY_ASSIGNED_CONTEXT ( ( #13740 ) ) GLOBAL_UNIT_ASSIGNED_CONTEXT ( ( #165, #15668, #15396 ) ) REPRESENTATION_CONTEXT ( 'NONE', 'WORKASPACE' ) );
#11686=PRODUCT_DEFINITION_CONTEXT ( 'detailed design', #13746, 'design' ) ;
#11745=ADVANCED_FACE ( 'NONE', ( #5355 ), #8992, .T. ) ;
#11921=CARTESIAN_POINT ( 'NONE',  ( -10.40000000000000036, 0.000000000000000000, 0.000000000000000000 ) ) ;
#12003=CARTESIAN_POINT ( 'NONE',  ( -10.40000000000000036, 0.000000000000000000, 0.000000000000000000 ) ) ;
#12244=TOROIDAL_SURFACE ( 'NONE', #6453, 10.40000000000000036, 0.9000000000000003553 ) ;
#12290=FACE_OUTER_BOUND ( 'NONE', #12406, .T. ) ;
#12337=PRODUCT_DEFINITION ( 'UNKNOWN', '', #11179, #11686 ) ;
#12406=EDGE_LOOP ( 'NONE', ( #211, #3622, #433, #14660 ) ) ;
#12436=DIRECTION ( 'NONE',  ( -0.000000000000000000, -0.000000000000000000, -1.000000000000000000 ) ) ;
#12442=AXIS2_PLACEMENT_3D ( 'NONE', #15539, #3122, #7214 ) ;
#12764=AXIS2_PLACEMENT_3D ( 'NONE', #9244, #14790, #6449 ) ;
#12833=PRODUCT_CONTEXT ( 'NONE', #13956, 'mechanical' ) ;
#12860=( LENGTH_UNIT ( ) NAMED_UNIT ( * ) SI_UNIT ( .MILLI., .METRE. ) );
#12997=ORIENTED_EDGE ( 'NONE', *, *, #8405, .F. ) ;
#13112=EDGE_LOOP ( 'NONE', ( #2749, #13474, #7197, #986 ) ) ;
#13304=PRODUCT ( 'o-rings series a_iso_O-ring 19x1.8-A-ISO 3601-1', 'o-rings series a_iso_O-ring 19x1.8-A-ISO 3601-1', '', ( #12833 ) ) ;
#13474=ORIENTED_EDGE ( 'NONE', *, *, #3875, .F. ) ;
#13617=DIRECTION ( 'NONE',  ( -1.000000000000000000, 0.000000000000000000, 0.000000000000000000 ) ) ;
#13720=CARTESIAN_POINT ( 'NONE',  ( 0.000000000000000000, 0.000000000000000000, 0.000000000000000000 ) ) ;
#13740=UNCERTAINTY_MEASURE_WITH_UNIT (LENGTH_MEASURE( 1.000000000000000082E-05 ), #165, 'distance_accuracy_value', 'NONE');
#13746=APPLICATION_CONTEXT ( 'automotive_design' ) ;
#13900=CLOSED_SHELL ( 'NONE', ( #15933, #11745, #11133, #9436 ) ) ;
#13956=APPLICATION_CONTEXT ( 'automotive_design' ) ;
#13971=CARTESIAN_POINT ( 'NONE',  ( 0.000000000000000000, 0.000000000000000000, 0.000000000000000000 ) ) ;
#14039=SURFACE_STYLE_USAGE ( .BOTH. , #16954 ) ;
#14045=VERTEX_POINT ( 'NONE', #2411 ) ;
#14057=UNCERTAINTY_MEASURE_WITH_UNIT (LENGTH_MEASURE( 1.000000000000000082E-05 ), #7945, 'distance_accuracy_value', 'NONE');
#14107=CIRCLE ( 'NONE', #14973, 0.9000000000000003553 ) ;
#14172=ORIENTED_EDGE ( 'NONE', *, *, #10518, .F. ) ;
#14276=AXIS2_PLACEMENT_3D ( 'NONE', #11921, #3604, #17593 ) ;
#14401=FILL_AREA_STYLE ('',( #9937 ) ) ;
#14616=ADVANCED_BREP_SHAPE_REPRESENTATION ( '', ( #17490, #3575 ), #11602 ) ;
#14653=DIRECTION ( 'NONE',  ( 0.000000000000000000, -1.000000000000000000, 0.000000000000000000 ) ) ;
#14660=ORIENTED_EDGE ( 'NONE', *, *, #686, .F. ) ;
#14719=CARTESIAN_POINT ( 'NONE',  ( 11.29999999999999893, 1.383850883036509067E-15, 0.000000000000000000 ) ) ;
#14790=DIRECTION ( 'NONE',  ( -0.000000000000000000, -0.000000000000000000, -1.000000000000000000 ) ) ;
#14803=( GEOMETRIC_REPRESENTATION_CONTEXT ( 3 ) GLOBAL_UNCERTAINTY_ASSIGNED_CONTEXT ( ( #4134 ) ) GLOBAL_UNIT_ASSIGNED_CONTEXT ( ( #12860, #7156, #526 ) ) REPRESENTATION_CONTEXT ( 'NONE', 'WORKASPACE' ) );
#14973=AXIS2_PLACEMENT_3D ( 'NONE', #12003, #14653, #1043 ) ;
#15377=CIRCLE ( 'NONE', #12764, 9.500000000000000000 ) ;
#15396=( NAMED_UNIT ( * ) SI_UNIT ( $, .STERADIAN. ) SOLID_ANGLE_UNIT ( ) );
#15539=CARTESIAN_POINT ( 'NONE',  ( 10.40000000000000036, 1.273632671113247276E-15, 0.000000000000000000 ) ) ;
#15635=CIRCLE ( 'NONE', #12442, 0.8999999999999998002 ) ;
#15668=( NAMED_UNIT ( * ) PLANE_ANGLE_UNIT ( ) SI_UNIT ( $, .RADIAN. ) );
#15933=ADVANCED_FACE ( 'NONE', ( #12290 ), #12244, .T. ) ;
#16259=CIRCLE ( 'NONE', #898, 9.500000000000000000 ) ;
#16433=EDGE_CURVE ( 'NONE', #14045, #11061, #7309, .T. ) ;
#16657=EDGE_CURVE ( 'NONE', #11061, #133, #8497, .T. ) ;
#16954=SURFACE_SIDE_STYLE ('',( #8589 ) ) ;
#17041=SHAPE_REPRESENTATION_RELATIONSHIP ( 'NONE' , 'NONE' ,  #2081, #14616 ) ;
#17193=CIRCLE ( 'NONE', #14276, 0.9000000000000003553 ) ;
#17490=MANIFOLD_SOLID_BREP ( 'Sweep1', #13900 ) ;
#17513=FILL_AREA_STYLE ('',( #5202 ) ) ;
#17575=DIRECTION ( 'NONE',  ( 0.000000000000000000, 0.000000000000000000, 1.000000000000000000 ) ) ;
#17593=DIRECTION ( 'NONE',  ( 0.000000000000000000, 0.000000000000000000, -1.000000000000000000 ) ) ;
#17800=CARTESIAN_POINT ( 'NONE',  ( 10.40000000000000036, 1.273632671113247276E-15, 0.000000000000000000 ) ) ;
ENDSEC;
END-ISO-10303-21;
